ISO-10303-21;
HEADER;
/* Generated by software containing ST-Developer
 * from STEP Tools, Inc. (www.steptools.com) 
 */

FILE_DESCRIPTION(
/* description */ ('Two-link friction support arm'),
/* implementation_level */ '2;1');

FILE_NAME(
/* name */ 'Captive-nut hand knob.step',
/* time_stamp */ '2026-10-27T20:01:49-07:00',
/* author */ (''),
/* organization */ (''),
/* preprocessor_version */ 'ST-DEVELOPER v20.2',
/* originating_system */ 'Autodesk Translation Framework v15.17.0.0',
/* authorisation */ '');

FILE_SCHEMA (('AUTOMOTIVE_DESIGN { 1 0 10303 214 3 1 1 }'));
ENDSEC;

DATA;
#10=MECHANICAL_DESIGN_GEOMETRIC_PRESENTATION_REPRESENTATION('',(#205),#5492);
#183=SHAPE_REPRESENTATION_RELATIONSHIP('SRR','None',#5577,#194);
#194=ADVANCED_BREP_SHAPE_REPRESENTATION('',(#215),#5491);
#205=STYLED_ITEM('',(#5708),#215);
#215=MANIFOLD_SOLID_BREP('Body1',#3182);
#247=FACE_BOUND('',#723,.T.);
#248=FACE_BOUND('',#737,.T.);
#249=FACE_BOUND('',#740,.T.);
#364=PLANE('',#3551);
#365=PLANE('',#3571);
#366=PLANE('',#3572);
#367=PLANE('',#3573);
#368=PLANE('',#3574);
#369=PLANE('',#3575);
#370=PLANE('',#3576);
#371=PLANE('',#3577);
#372=PLANE('',#3580);
#518=FACE_OUTER_BOUND('',#716,.T.);
#519=FACE_OUTER_BOUND('',#717,.T.);
#520=FACE_OUTER_BOUND('',#718,.T.);
#521=FACE_OUTER_BOUND('',#719,.T.);
#522=FACE_OUTER_BOUND('',#720,.T.);
#523=FACE_OUTER_BOUND('',#721,.T.);
#524=FACE_OUTER_BOUND('',#722,.T.);
#525=FACE_OUTER_BOUND('',#724,.T.);
#526=FACE_OUTER_BOUND('',#725,.T.);
#527=FACE_OUTER_BOUND('',#726,.T.);
#528=FACE_OUTER_BOUND('',#727,.T.);
#529=FACE_OUTER_BOUND('',#728,.T.);
#530=FACE_OUTER_BOUND('',#729,.T.);
#531=FACE_OUTER_BOUND('',#730,.T.);
#532=FACE_OUTER_BOUND('',#731,.T.);
#533=FACE_OUTER_BOUND('',#732,.T.);
#534=FACE_OUTER_BOUND('',#733,.T.);
#535=FACE_OUTER_BOUND('',#734,.T.);
#536=FACE_OUTER_BOUND('',#735,.T.);
#537=FACE_OUTER_BOUND('',#736,.T.);
#538=FACE_OUTER_BOUND('',#738,.T.);
#539=FACE_OUTER_BOUND('',#739,.T.);
#716=EDGE_LOOP('',(#2854,#2855,#2856,#2857));
#717=EDGE_LOOP('',(#2858,#2859,#2860,#2861));
#718=EDGE_LOOP('',(#2862,#2863,#2864,#2865));
#719=EDGE_LOOP('',(#2866,#2867,#2868,#2869));
#720=EDGE_LOOP('',(#2870,#2871,#2872,#2873));
#721=EDGE_LOOP('',(#2874,#2875,#2876,#2877));
#722=EDGE_LOOP('',(#2878,#2879,#2880,#2881,#2882,#2883,#2884,#2885,#2886,
#2887,#2888,#2889));
#723=EDGE_LOOP('',(#2890));
#724=EDGE_LOOP('',(#2891,#2892,#2893,#2894));
#725=EDGE_LOOP('',(#2895,#2896,#2897,#2898));
#726=EDGE_LOOP('',(#2899,#2900,#2901,#2902));
#727=EDGE_LOOP('',(#2903,#2904,#2905,#2906));
#728=EDGE_LOOP('',(#2907,#2908,#2909,#2910));
#729=EDGE_LOOP('',(#2911,#2912,#2913,#2914));
#730=EDGE_LOOP('',(#2915,#2916,#2917,#2918));
#731=EDGE_LOOP('',(#2919,#2920,#2921,#2922));
#732=EDGE_LOOP('',(#2923,#2924,#2925,#2926));
#733=EDGE_LOOP('',(#2927,#2928,#2929,#2930));
#734=EDGE_LOOP('',(#2931,#2932,#2933,#2934));
#735=EDGE_LOOP('',(#2935,#2936,#2937,#2938));
#736=EDGE_LOOP('',(#2939,#2940,#2941,#2942,#2943,#2944));
#737=EDGE_LOOP('',(#2945));
#738=EDGE_LOOP('',(#2946,#2947,#2948,#2949));
#739=EDGE_LOOP('',(#2950,#2951,#2952,#2953,#2954,#2955,#2956,#2957,#2958,
#2959,#2960,#2961));
#740=EDGE_LOOP('',(#2962,#2963,#2964,#2965,#2966,#2967));
#1023=LINE('',#5321,#1336);
#1024=LINE('',#5325,#1337);
#1025=LINE('',#5330,#1338);
#1026=LINE('',#5334,#1339);
#1027=LINE('',#5339,#1340);
#1028=LINE('',#5343,#1341);
#1029=LINE('',#5348,#1342);
#1030=LINE('',#5352,#1343);
#1031=LINE('',#5357,#1344);
#1032=LINE('',#5361,#1345);
#1033=LINE('',#5366,#1346);
#1034=LINE('',#5370,#1347);
#1035=LINE('',#5396,#1348);
#1036=LINE('',#5398,#1349);
#1037=LINE('',#5400,#1350);
#1038=LINE('',#5401,#1351);
#1039=LINE('',#5404,#1352);
#1040=LINE('',#5406,#1353);
#1041=LINE('',#5407,#1354);
#1042=LINE('',#5410,#1355);
#1043=LINE('',#5412,#1356);
#1044=LINE('',#5413,#1357);
#1045=LINE('',#5416,#1358);
#1046=LINE('',#5418,#1359);
#1047=LINE('',#5419,#1360);
#1048=LINE('',#5422,#1361);
#1049=LINE('',#5424,#1362);
#1050=LINE('',#5425,#1363);
#1051=LINE('',#5427,#1364);
#1052=LINE('',#5428,#1365);
#1053=LINE('',#5433,#1366);
#1336=VECTOR('',#4345,1.);
#1337=VECTOR('',#4348,1.);
#1338=VECTOR('',#4353,1.);
#1339=VECTOR('',#4356,1.);
#1340=VECTOR('',#4361,1.);
#1341=VECTOR('',#4364,1.);
#1342=VECTOR('',#4369,1.);
#1343=VECTOR('',#4372,1.);
#1344=VECTOR('',#4377,1.);
#1345=VECTOR('',#4380,1.);
#1346=VECTOR('',#4385,1.);
#1347=VECTOR('',#4388,1.);
#1348=VECTOR('',#4433,1.);
#1349=VECTOR('',#4434,1.);
#1350=VECTOR('',#4435,1.);
#1351=VECTOR('',#4436,1.);
#1352=VECTOR('',#4439,1.);
#1353=VECTOR('',#4440,1.);
#1354=VECTOR('',#4441,1.);
#1355=VECTOR('',#4444,1.);
#1356=VECTOR('',#4445,1.);
#1357=VECTOR('',#4446,1.);
#1358=VECTOR('',#4449,1.);
#1359=VECTOR('',#4450,1.);
#1360=VECTOR('',#4451,1.);
#1361=VECTOR('',#4454,1.);
#1362=VECTOR('',#4455,1.);
#1363=VECTOR('',#4456,1.);
#1364=VECTOR('',#4459,1.);
#1365=VECTOR('',#4460,1.);
#1366=VECTOR('',#4467,0.425);
#1423=CIRCLE('',#3534,0.4);
#1424=CIRCLE('',#3535,0.4);
#1425=CIRCLE('',#3537,0.4);
#1426=CIRCLE('',#3538,0.4);
#1427=CIRCLE('',#3540,0.4);
#1428=CIRCLE('',#3541,0.4);
#1429=CIRCLE('',#3543,0.4);
#1430=CIRCLE('',#3544,0.4);
#1431=CIRCLE('',#3546,0.4);
#1432=CIRCLE('',#3547,0.4);
#1433=CIRCLE('',#3549,0.4);
#1434=CIRCLE('',#3550,0.4);
#1435=CIRCLE('',#3552,1.8);
#1436=CIRCLE('',#3553,1.8);
#1437=CIRCLE('',#3554,1.8);
#1438=CIRCLE('',#3555,1.8);
#1439=CIRCLE('',#3556,1.8);
#1440=CIRCLE('',#3557,1.8);
#1441=CIRCLE('',#3558,0.425);
#1442=CIRCLE('',#3560,1.8);
#1443=CIRCLE('',#3562,1.8);
#1444=CIRCLE('',#3564,1.8);
#1445=CIRCLE('',#3566,1.8);
#1446=CIRCLE('',#3568,1.8);
#1447=CIRCLE('',#3570,1.8);
#1448=CIRCLE('',#3578,0.425);
#1685=VERTEX_POINT('',#5319);
#1686=VERTEX_POINT('',#5320);
#1687=VERTEX_POINT('',#5322);
#1688=VERTEX_POINT('',#5324);
#1689=VERTEX_POINT('',#5328);
#1690=VERTEX_POINT('',#5329);
#1691=VERTEX_POINT('',#5331);
#1692=VERTEX_POINT('',#5333);
#1693=VERTEX_POINT('',#5337);
#1694=VERTEX_POINT('',#5338);
#1695=VERTEX_POINT('',#5340);
#1696=VERTEX_POINT('',#5342);
#1697=VERTEX_POINT('',#5346);
#1698=VERTEX_POINT('',#5347);
#1699=VERTEX_POINT('',#5349);
#1700=VERTEX_POINT('',#5351);
#1701=VERTEX_POINT('',#5355);
#1702=VERTEX_POINT('',#5356);
#1703=VERTEX_POINT('',#5358);
#1704=VERTEX_POINT('',#5360);
#1705=VERTEX_POINT('',#5364);
#1706=VERTEX_POINT('',#5365);
#1707=VERTEX_POINT('',#5367);
#1708=VERTEX_POINT('',#5369);
#1709=VERTEX_POINT('',#5379);
#1710=VERTEX_POINT('',#5394);
#1711=VERTEX_POINT('',#5395);
#1712=VERTEX_POINT('',#5397);
#1713=VERTEX_POINT('',#5399);
#1714=VERTEX_POINT('',#5403);
#1715=VERTEX_POINT('',#5405);
#1716=VERTEX_POINT('',#5409);
#1717=VERTEX_POINT('',#5411);
#1718=VERTEX_POINT('',#5415);
#1719=VERTEX_POINT('',#5417);
#1720=VERTEX_POINT('',#5421);
#1721=VERTEX_POINT('',#5423);
#1722=VERTEX_POINT('',#5430);
#2081=EDGE_CURVE('',#1685,#1686,#1023,.T.);
#2082=EDGE_CURVE('',#1687,#1685,#1423,.T.);
#2083=EDGE_CURVE('',#1688,#1687,#1024,.T.);
#2084=EDGE_CURVE('',#1686,#1688,#1424,.T.);
#2085=EDGE_CURVE('',#1689,#1690,#1025,.T.);
#2086=EDGE_CURVE('',#1691,#1689,#1425,.T.);
#2087=EDGE_CURVE('',#1692,#1691,#1026,.T.);
#2088=EDGE_CURVE('',#1690,#1692,#1426,.T.);
#2089=EDGE_CURVE('',#1693,#1694,#1027,.T.);
#2090=EDGE_CURVE('',#1695,#1693,#1427,.T.);
#2091=EDGE_CURVE('',#1696,#1695,#1028,.T.);
#2092=EDGE_CURVE('',#1694,#1696,#1428,.T.);
#2093=EDGE_CURVE('',#1697,#1698,#1029,.T.);
#2094=EDGE_CURVE('',#1699,#1697,#1429,.T.);
#2095=EDGE_CURVE('',#1700,#1699,#1030,.T.);
#2096=EDGE_CURVE('',#1698,#1700,#1430,.T.);
#2097=EDGE_CURVE('',#1701,#1702,#1031,.T.);
#2098=EDGE_CURVE('',#1703,#1701,#1431,.T.);
#2099=EDGE_CURVE('',#1704,#1703,#1032,.T.);
#2100=EDGE_CURVE('',#1702,#1704,#1432,.T.);
#2101=EDGE_CURVE('',#1705,#1706,#1033,.T.);
#2102=EDGE_CURVE('',#1707,#1705,#1433,.T.);
#2103=EDGE_CURVE('',#1708,#1707,#1034,.T.);
#2104=EDGE_CURVE('',#1706,#1708,#1434,.T.);
#2105=EDGE_CURVE('',#1685,#1707,#1435,.T.);
#2106=EDGE_CURVE('',#1705,#1690,#1436,.T.);
#2107=EDGE_CURVE('',#1692,#1695,#1437,.T.);
#2108=EDGE_CURVE('',#1693,#1699,#1438,.T.);
#2109=EDGE_CURVE('',#1697,#1703,#1439,.T.);
#2110=EDGE_CURVE('',#1701,#1687,#1440,.T.);
#2111=EDGE_CURVE('',#1709,#1709,#1441,.T.);
#2112=EDGE_CURVE('',#1698,#1704,#1442,.T.);
#2113=EDGE_CURVE('',#1694,#1700,#1443,.T.);
#2114=EDGE_CURVE('',#1706,#1689,#1444,.T.);
#2115=EDGE_CURVE('',#1691,#1696,#1445,.T.);
#2116=EDGE_CURVE('',#1686,#1708,#1446,.T.);
#2117=EDGE_CURVE('',#1702,#1688,#1447,.T.);
#2118=EDGE_CURVE('',#1710,#1711,#1035,.T.);
#2119=EDGE_CURVE('',#1710,#1712,#1036,.T.);
#2120=EDGE_CURVE('',#1712,#1713,#1037,.T.);
#2121=EDGE_CURVE('',#1711,#1713,#1038,.T.);
#2122=EDGE_CURVE('',#1711,#1714,#1039,.T.);
#2123=EDGE_CURVE('',#1713,#1715,#1040,.T.);
#2124=EDGE_CURVE('',#1714,#1715,#1041,.T.);
#2125=EDGE_CURVE('',#1714,#1716,#1042,.T.);
#2126=EDGE_CURVE('',#1715,#1717,#1043,.T.);
#2127=EDGE_CURVE('',#1716,#1717,#1044,.T.);
#2128=EDGE_CURVE('',#1716,#1718,#1045,.T.);
#2129=EDGE_CURVE('',#1717,#1719,#1046,.T.);
#2130=EDGE_CURVE('',#1718,#1719,#1047,.T.);
#2131=EDGE_CURVE('',#1720,#1710,#1048,.T.);
#2132=EDGE_CURVE('',#1720,#1721,#1049,.T.);
#2133=EDGE_CURVE('',#1721,#1712,#1050,.T.);
#2134=EDGE_CURVE('',#1718,#1720,#1051,.T.);
#2135=EDGE_CURVE('',#1719,#1721,#1052,.T.);
#2136=EDGE_CURVE('',#1722,#1722,#1448,.T.);
#2137=EDGE_CURVE('',#1709,#1722,#1053,.T.);
#2854=ORIENTED_EDGE('',*,*,#2081,.F.);
#2855=ORIENTED_EDGE('',*,*,#2082,.F.);
#2856=ORIENTED_EDGE('',*,*,#2083,.F.);
#2857=ORIENTED_EDGE('',*,*,#2084,.F.);
#2858=ORIENTED_EDGE('',*,*,#2085,.F.);
#2859=ORIENTED_EDGE('',*,*,#2086,.F.);
#2860=ORIENTED_EDGE('',*,*,#2087,.F.);
#2861=ORIENTED_EDGE('',*,*,#2088,.F.);
#2862=ORIENTED_EDGE('',*,*,#2089,.F.);
#2863=ORIENTED_EDGE('',*,*,#2090,.F.);
#2864=ORIENTED_EDGE('',*,*,#2091,.F.);
#2865=ORIENTED_EDGE('',*,*,#2092,.F.);
#2866=ORIENTED_EDGE('',*,*,#2093,.F.);
#2867=ORIENTED_EDGE('',*,*,#2094,.F.);
#2868=ORIENTED_EDGE('',*,*,#2095,.F.);
#2869=ORIENTED_EDGE('',*,*,#2096,.F.);
#2870=ORIENTED_EDGE('',*,*,#2097,.F.);
#2871=ORIENTED_EDGE('',*,*,#2098,.F.);
#2872=ORIENTED_EDGE('',*,*,#2099,.F.);
#2873=ORIENTED_EDGE('',*,*,#2100,.F.);
#2874=ORIENTED_EDGE('',*,*,#2101,.F.);
#2875=ORIENTED_EDGE('',*,*,#2102,.F.);
#2876=ORIENTED_EDGE('',*,*,#2103,.F.);
#2877=ORIENTED_EDGE('',*,*,#2104,.F.);
#2878=ORIENTED_EDGE('',*,*,#2082,.T.);
#2879=ORIENTED_EDGE('',*,*,#2105,.T.);
#2880=ORIENTED_EDGE('',*,*,#2102,.T.);
#2881=ORIENTED_EDGE('',*,*,#2106,.T.);
#2882=ORIENTED_EDGE('',*,*,#2088,.T.);
#2883=ORIENTED_EDGE('',*,*,#2107,.T.);
#2884=ORIENTED_EDGE('',*,*,#2090,.T.);
#2885=ORIENTED_EDGE('',*,*,#2108,.T.);
#2886=ORIENTED_EDGE('',*,*,#2094,.T.);
#2887=ORIENTED_EDGE('',*,*,#2109,.T.);
#2888=ORIENTED_EDGE('',*,*,#2098,.T.);
#2889=ORIENTED_EDGE('',*,*,#2110,.T.);
#2890=ORIENTED_EDGE('',*,*,#2111,.T.);
#2891=ORIENTED_EDGE('',*,*,#2093,.T.);
#2892=ORIENTED_EDGE('',*,*,#2112,.T.);
#2893=ORIENTED_EDGE('',*,*,#2099,.T.);
#2894=ORIENTED_EDGE('',*,*,#2109,.F.);
#2895=ORIENTED_EDGE('',*,*,#2089,.T.);
#2896=ORIENTED_EDGE('',*,*,#2113,.T.);
#2897=ORIENTED_EDGE('',*,*,#2095,.T.);
#2898=ORIENTED_EDGE('',*,*,#2108,.F.);
#2899=ORIENTED_EDGE('',*,*,#2085,.T.);
#2900=ORIENTED_EDGE('',*,*,#2106,.F.);
#2901=ORIENTED_EDGE('',*,*,#2101,.T.);
#2902=ORIENTED_EDGE('',*,*,#2114,.T.);
#2903=ORIENTED_EDGE('',*,*,#2087,.T.);
#2904=ORIENTED_EDGE('',*,*,#2115,.T.);
#2905=ORIENTED_EDGE('',*,*,#2091,.T.);
#2906=ORIENTED_EDGE('',*,*,#2107,.F.);
#2907=ORIENTED_EDGE('',*,*,#2081,.T.);
#2908=ORIENTED_EDGE('',*,*,#2116,.T.);
#2909=ORIENTED_EDGE('',*,*,#2103,.T.);
#2910=ORIENTED_EDGE('',*,*,#2105,.F.);
#2911=ORIENTED_EDGE('',*,*,#2083,.T.);
#2912=ORIENTED_EDGE('',*,*,#2110,.F.);
#2913=ORIENTED_EDGE('',*,*,#2097,.T.);
#2914=ORIENTED_EDGE('',*,*,#2117,.T.);
#2915=ORIENTED_EDGE('',*,*,#2118,.F.);
#2916=ORIENTED_EDGE('',*,*,#2119,.T.);
#2917=ORIENTED_EDGE('',*,*,#2120,.T.);
#2918=ORIENTED_EDGE('',*,*,#2121,.F.);
#2919=ORIENTED_EDGE('',*,*,#2122,.F.);
#2920=ORIENTED_EDGE('',*,*,#2121,.T.);
#2921=ORIENTED_EDGE('',*,*,#2123,.T.);
#2922=ORIENTED_EDGE('',*,*,#2124,.F.);
#2923=ORIENTED_EDGE('',*,*,#2125,.F.);
#2924=ORIENTED_EDGE('',*,*,#2124,.T.);
#2925=ORIENTED_EDGE('',*,*,#2126,.T.);
#2926=ORIENTED_EDGE('',*,*,#2127,.F.);
#2927=ORIENTED_EDGE('',*,*,#2128,.F.);
#2928=ORIENTED_EDGE('',*,*,#2127,.T.);
#2929=ORIENTED_EDGE('',*,*,#2129,.T.);
#2930=ORIENTED_EDGE('',*,*,#2130,.F.);
#2931=ORIENTED_EDGE('',*,*,#2131,.F.);
#2932=ORIENTED_EDGE('',*,*,#2132,.T.);
#2933=ORIENTED_EDGE('',*,*,#2133,.T.);
#2934=ORIENTED_EDGE('',*,*,#2119,.F.);
#2935=ORIENTED_EDGE('',*,*,#2134,.F.);
#2936=ORIENTED_EDGE('',*,*,#2130,.T.);
#2937=ORIENTED_EDGE('',*,*,#2135,.T.);
#2938=ORIENTED_EDGE('',*,*,#2132,.F.);
#2939=ORIENTED_EDGE('',*,*,#2135,.F.);
#2940=ORIENTED_EDGE('',*,*,#2129,.F.);
#2941=ORIENTED_EDGE('',*,*,#2126,.F.);
#2942=ORIENTED_EDGE('',*,*,#2123,.F.);
#2943=ORIENTED_EDGE('',*,*,#2120,.F.);
#2944=ORIENTED_EDGE('',*,*,#2133,.F.);
#2945=ORIENTED_EDGE('',*,*,#2136,.F.);
#2946=ORIENTED_EDGE('',*,*,#2111,.F.);
#2947=ORIENTED_EDGE('',*,*,#2137,.T.);
#2948=ORIENTED_EDGE('',*,*,#2136,.T.);
#2949=ORIENTED_EDGE('',*,*,#2137,.F.);
#2950=ORIENTED_EDGE('',*,*,#2084,.T.);
#2951=ORIENTED_EDGE('',*,*,#2117,.F.);
#2952=ORIENTED_EDGE('',*,*,#2100,.T.);
#2953=ORIENTED_EDGE('',*,*,#2112,.F.);
#2954=ORIENTED_EDGE('',*,*,#2096,.T.);
#2955=ORIENTED_EDGE('',*,*,#2113,.F.);
#2956=ORIENTED_EDGE('',*,*,#2092,.T.);
#2957=ORIENTED_EDGE('',*,*,#2115,.F.);
#2958=ORIENTED_EDGE('',*,*,#2086,.T.);
#2959=ORIENTED_EDGE('',*,*,#2114,.F.);
#2960=ORIENTED_EDGE('',*,*,#2104,.T.);
#2961=ORIENTED_EDGE('',*,*,#2116,.F.);
#2962=ORIENTED_EDGE('',*,*,#2128,.T.);
#2963=ORIENTED_EDGE('',*,*,#2134,.T.);
#2964=ORIENTED_EDGE('',*,*,#2131,.T.);
#2965=ORIENTED_EDGE('',*,*,#2118,.T.);
#2966=ORIENTED_EDGE('',*,*,#2122,.T.);
#2967=ORIENTED_EDGE('',*,*,#2125,.T.);
#2991=CYLINDRICAL_SURFACE('',#3533,0.4);
#2992=CYLINDRICAL_SURFACE('',#3536,0.4);
#2993=CYLINDRICAL_SURFACE('',#3539,0.4);
#2994=CYLINDRICAL_SURFACE('',#3542,0.4);
#2995=CYLINDRICAL_SURFACE('',#3545,0.4);
#2996=CYLINDRICAL_SURFACE('',#3548,0.4);
#2997=CYLINDRICAL_SURFACE('',#3559,1.8);
#2998=CYLINDRICAL_SURFACE('',#3561,1.8);
#2999=CYLINDRICAL_SURFACE('',#3563,1.8);
#3000=CYLINDRICAL_SURFACE('',#3565,1.8);
#3001=CYLINDRICAL_SURFACE('',#3567,1.8);
#3002=CYLINDRICAL_SURFACE('',#3569,1.8);
#3003=CYLINDRICAL_SURFACE('',#3579,0.425);
#3149=ADVANCED_FACE('',(#518),#2991,.F.);
#3150=ADVANCED_FACE('',(#519),#2992,.F.);
#3151=ADVANCED_FACE('',(#520),#2993,.F.);
#3152=ADVANCED_FACE('',(#521),#2994,.F.);
#3153=ADVANCED_FACE('',(#522),#2995,.F.);
#3154=ADVANCED_FACE('',(#523),#2996,.F.);
#3155=ADVANCED_FACE('',(#524,#247),#364,.T.);
#3156=ADVANCED_FACE('',(#525),#2997,.T.);
#3157=ADVANCED_FACE('',(#526),#2998,.T.);
#3158=ADVANCED_FACE('',(#527),#2999,.T.);
#3159=ADVANCED_FACE('',(#528),#3000,.T.);
#3160=ADVANCED_FACE('',(#529),#3001,.T.);
#3161=ADVANCED_FACE('',(#530),#3002,.T.);
#3162=ADVANCED_FACE('',(#531),#365,.F.);
#3163=ADVANCED_FACE('',(#532),#366,.F.);
#3164=ADVANCED_FACE('',(#533),#367,.F.);
#3165=ADVANCED_FACE('',(#534),#368,.F.);
#3166=ADVANCED_FACE('',(#535),#369,.F.);
#3167=ADVANCED_FACE('',(#536),#370,.F.);
#3168=ADVANCED_FACE('',(#537,#248),#371,.F.);
#3169=ADVANCED_FACE('',(#538),#3003,.F.);
#3170=ADVANCED_FACE('',(#539,#249),#372,.F.);
#3182=CLOSED_SHELL('',(#3149,#3150,#3151,#3152,#3153,#3154,#3155,#3156,
#3157,#3158,#3159,#3160,#3161,#3162,#3163,#3164,#3165,#3166,#3167,#3168,
#3169,#3170));
#3532=AXIS2_PLACEMENT_3D('',#5317,#4341,#4342);
#3533=AXIS2_PLACEMENT_3D('',#5318,#4343,#4344);
#3534=AXIS2_PLACEMENT_3D('',#5323,#4346,#4347);
#3535=AXIS2_PLACEMENT_3D('',#5326,#4349,#4350);
#3536=AXIS2_PLACEMENT_3D('',#5327,#4351,#4352);
#3537=AXIS2_PLACEMENT_3D('',#5332,#4354,#4355);
#3538=AXIS2_PLACEMENT_3D('',#5335,#4357,#4358);
#3539=AXIS2_PLACEMENT_3D('',#5336,#4359,#4360);
#3540=AXIS2_PLACEMENT_3D('',#5341,#4362,#4363);
#3541=AXIS2_PLACEMENT_3D('',#5344,#4365,#4366);
#3542=AXIS2_PLACEMENT_3D('',#5345,#4367,#4368);
#3543=AXIS2_PLACEMENT_3D('',#5350,#4370,#4371);
#3544=AXIS2_PLACEMENT_3D('',#5353,#4373,#4374);
#3545=AXIS2_PLACEMENT_3D('',#5354,#4375,#4376);
#3546=AXIS2_PLACEMENT_3D('',#5359,#4378,#4379);
#3547=AXIS2_PLACEMENT_3D('',#5362,#4381,#4382);
#3548=AXIS2_PLACEMENT_3D('',#5363,#4383,#4384);
#3549=AXIS2_PLACEMENT_3D('',#5368,#4386,#4387);
#3550=AXIS2_PLACEMENT_3D('',#5371,#4389,#4390);
#3551=AXIS2_PLACEMENT_3D('',#5372,#4391,#4392);
#3552=AXIS2_PLACEMENT_3D('',#5373,#4393,#4394);
#3553=AXIS2_PLACEMENT_3D('',#5374,#4395,#4396);
#3554=AXIS2_PLACEMENT_3D('',#5375,#4397,#4398);
#3555=AXIS2_PLACEMENT_3D('',#5376,#4399,#4400);
#3556=AXIS2_PLACEMENT_3D('',#5377,#4401,#4402);
#3557=AXIS2_PLACEMENT_3D('',#5378,#4403,#4404);
#3558=AXIS2_PLACEMENT_3D('',#5380,#4405,#4406);
#3559=AXIS2_PLACEMENT_3D('',#5381,#4407,#4408);
#3560=AXIS2_PLACEMENT_3D('',#5382,#4409,#4410);
#3561=AXIS2_PLACEMENT_3D('',#5383,#4411,#4412);
#3562=AXIS2_PLACEMENT_3D('',#5384,#4413,#4414);
#3563=AXIS2_PLACEMENT_3D('',#5385,#4415,#4416);
#3564=AXIS2_PLACEMENT_3D('',#5386,#4417,#4418);
#3565=AXIS2_PLACEMENT_3D('',#5387,#4419,#4420);
#3566=AXIS2_PLACEMENT_3D('',#5388,#4421,#4422);
#3567=AXIS2_PLACEMENT_3D('',#5389,#4423,#4424);
#3568=AXIS2_PLACEMENT_3D('',#5390,#4425,#4426);
#3569=AXIS2_PLACEMENT_3D('',#5391,#4427,#4428);
#3570=AXIS2_PLACEMENT_3D('',#5392,#4429,#4430);
#3571=AXIS2_PLACEMENT_3D('',#5393,#4431,#4432);
#3572=AXIS2_PLACEMENT_3D('',#5402,#4437,#4438);
#3573=AXIS2_PLACEMENT_3D('',#5408,#4442,#4443);
#3574=AXIS2_PLACEMENT_3D('',#5414,#4447,#4448);
#3575=AXIS2_PLACEMENT_3D('',#5420,#4452,#4453);
#3576=AXIS2_PLACEMENT_3D('',#5426,#4457,#4458);
#3577=AXIS2_PLACEMENT_3D('',#5429,#4461,#4462);
#3578=AXIS2_PLACEMENT_3D('',#5431,#4463,#4464);
#3579=AXIS2_PLACEMENT_3D('',#5432,#4465,#4466);
#3580=AXIS2_PLACEMENT_3D('',#5434,#4468,#4469);
#4341=DIRECTION('axis',(0.,0.,1.));
#4342=DIRECTION('refdir',(1.,0.,0.));
#4343=DIRECTION('center_axis',(0.,0.,1.));
#4344=DIRECTION('ref_axis',(1.,0.,0.));
#4345=DIRECTION('',(0.,0.,-1.));
#4346=DIRECTION('center_axis',(0.,0.,-1.));
#4347=DIRECTION('ref_axis',(1.,0.,0.));
#4348=DIRECTION('',(0.,0.,1.));
#4349=DIRECTION('center_axis',(0.,0.,1.));
#4350=DIRECTION('ref_axis',(1.,0.,0.));
#4351=DIRECTION('center_axis',(0.,0.,1.));
#4352=DIRECTION('ref_axis',(-1.,-1.22464679914735E-16,0.));
#4353=DIRECTION('',(0.,0.,1.));
#4354=DIRECTION('center_axis',(0.,0.,1.));
#4355=DIRECTION('ref_axis',(1.,0.,0.));
#4356=DIRECTION('',(0.,0.,-1.));
#4357=DIRECTION('center_axis',(0.,0.,-1.));
#4358=DIRECTION('ref_axis',(1.,0.,0.));
#4359=DIRECTION('center_axis',(0.,0.,1.));
#4360=DIRECTION('ref_axis',(1.,0.,0.));
#4361=DIRECTION('',(0.,0.,-1.));
#4362=DIRECTION('center_axis',(0.,0.,-1.));
#4363=DIRECTION('ref_axis',(1.,0.,0.));
#4364=DIRECTION('',(0.,0.,1.));
#4365=DIRECTION('center_axis',(0.,0.,1.));
#4366=DIRECTION('ref_axis',(1.,0.,0.));
#4367=DIRECTION('center_axis',(0.,0.,1.));
#4368=DIRECTION('ref_axis',(1.,0.,0.));
#4369=DIRECTION('',(0.,0.,-1.));
#4370=DIRECTION('center_axis',(0.,0.,-1.));
#4371=DIRECTION('ref_axis',(1.,0.,0.));
#4372=DIRECTION('',(0.,0.,1.));
#4373=DIRECTION('center_axis',(0.,0.,1.));
#4374=DIRECTION('ref_axis',(1.,0.,0.));
#4375=DIRECTION('center_axis',(0.,0.,1.));
#4376=DIRECTION('ref_axis',(1.,0.,0.));
#4377=DIRECTION('',(0.,0.,-1.));
#4378=DIRECTION('center_axis',(0.,0.,-1.));
#4379=DIRECTION('ref_axis',(1.,0.,0.));
#4380=DIRECTION('',(0.,0.,1.));
#4381=DIRECTION('center_axis',(0.,0.,1.));
#4382=DIRECTION('ref_axis',(1.,0.,0.));
#4383=DIRECTION('center_axis',(0.,0.,1.));
#4384=DIRECTION('ref_axis',(1.,0.,0.));
#4385=DIRECTION('',(0.,0.,-1.));
#4386=DIRECTION('center_axis',(0.,0.,-1.));
#4387=DIRECTION('ref_axis',(1.,0.,0.));
#4388=DIRECTION('',(0.,0.,1.));
#4389=DIRECTION('center_axis',(0.,0.,1.));
#4390=DIRECTION('ref_axis',(1.,0.,0.));
#4391=DIRECTION('center_axis',(0.,0.,1.));
#4392=DIRECTION('ref_axis',(1.,0.,0.));
#4393=DIRECTION('center_axis',(0.,0.,1.));
#4394=DIRECTION('ref_axis',(1.,0.,0.));
#4395=DIRECTION('center_axis',(0.,0.,1.));
#4396=DIRECTION('ref_axis',(1.,0.,0.));
#4397=DIRECTION('center_axis',(0.,0.,1.));
#4398=DIRECTION('ref_axis',(1.,0.,0.));
#4399=DIRECTION('center_axis',(0.,0.,1.));
#4400=DIRECTION('ref_axis',(1.,0.,0.));
#4401=DIRECTION('center_axis',(0.,0.,1.));
#4402=DIRECTION('ref_axis',(1.,0.,0.));
#4403=DIRECTION('center_axis',(0.,0.,1.));
#4404=DIRECTION('ref_axis',(1.,0.,0.));
#4405=DIRECTION('center_axis',(0.,0.,-1.));
#4406=DIRECTION('ref_axis',(1.,0.,0.));
#4407=DIRECTION('center_axis',(0.,0.,1.));
#4408=DIRECTION('ref_axis',(1.,0.,0.));
#4409=DIRECTION('center_axis',(0.,0.,1.));
#4410=DIRECTION('ref_axis',(1.,0.,0.));
#4411=DIRECTION('center_axis',(0.,0.,1.));
#4412=DIRECTION('ref_axis',(1.,0.,0.));
#4413=DIRECTION('center_axis',(0.,0.,1.));
#4414=DIRECTION('ref_axis',(1.,0.,0.));
#4415=DIRECTION('center_axis',(0.,0.,1.));
#4416=DIRECTION('ref_axis',(1.,0.,0.));
#4417=DIRECTION('center_axis',(0.,0.,1.));
#4418=DIRECTION('ref_axis',(1.,0.,0.));
#4419=DIRECTION('center_axis',(0.,0.,1.));
#4420=DIRECTION('ref_axis',(1.,0.,0.));
#4421=DIRECTION('center_axis',(0.,0.,1.));
#4422=DIRECTION('ref_axis',(1.,0.,0.));
#4423=DIRECTION('center_axis',(0.,0.,1.));
#4424=DIRECTION('ref_axis',(1.,0.,0.));
#4425=DIRECTION('center_axis',(0.,0.,1.));
#4426=DIRECTION('ref_axis',(1.,0.,0.));
#4427=DIRECTION('center_axis',(0.,0.,1.));
#4428=DIRECTION('ref_axis',(1.,0.,0.));
#4429=DIRECTION('center_axis',(0.,0.,1.));
#4430=DIRECTION('ref_axis',(1.,0.,0.));
#4431=DIRECTION('center_axis',(0.,1.,0.));
#4432=DIRECTION('ref_axis',(-1.,0.,0.));
#4433=DIRECTION('',(-1.,0.,0.));
#4434=DIRECTION('',(0.,0.,1.));
#4435=DIRECTION('',(-1.,0.,0.));
#4436=DIRECTION('',(0.,0.,1.));
#4437=DIRECTION('center_axis',(-0.866025403784438,0.500000000000001,0.));
#4438=DIRECTION('ref_axis',(-0.500000000000001,-0.866025403784438,0.));
#4439=DIRECTION('',(-0.500000000000001,-0.866025403784438,0.));
#4440=DIRECTION('',(-0.500000000000001,-0.866025403784438,0.));
#4441=DIRECTION('',(0.,0.,1.));
#4442=DIRECTION('center_axis',(-0.866025403784439,-0.5,0.));
#4443=DIRECTION('ref_axis',(0.5,-0.866025403784439,0.));
#4444=DIRECTION('',(0.5,-0.866025403784439,0.));
#4445=DIRECTION('',(0.5,-0.866025403784439,0.));
#4446=DIRECTION('',(0.,0.,1.));
#4447=DIRECTION('center_axis',(0.,-1.,0.));
#4448=DIRECTION('ref_axis',(1.,0.,0.));
#4449=DIRECTION('',(1.,0.,0.));
#4450=DIRECTION('',(1.,0.,0.));
#4451=DIRECTION('',(0.,0.,1.));
#4452=DIRECTION('center_axis',(0.866025403784439,0.5,0.));
#4453=DIRECTION('ref_axis',(-0.5,0.866025403784439,0.));
#4454=DIRECTION('',(-0.5,0.866025403784439,0.));
#4455=DIRECTION('',(0.,0.,1.));
#4456=DIRECTION('',(-0.5,0.866025403784439,0.));
#4457=DIRECTION('center_axis',(0.866025403784439,-0.5,0.));
#4458=DIRECTION('ref_axis',(0.5,0.866025403784439,0.));
#4459=DIRECTION('',(0.5,0.866025403784439,0.));
#4460=DIRECTION('',(0.5,0.866025403784439,0.));
#4461=DIRECTION('center_axis',(0.,0.,1.));
#4462=DIRECTION('ref_axis',(1.,0.,0.));
#4463=DIRECTION('center_axis',(0.,0.,-1.));
#4464=DIRECTION('ref_axis',(1.,0.,0.));
#4465=DIRECTION('center_axis',(0.,0.,1.));
#4466=DIRECTION('ref_axis',(1.,0.,0.));
#4467=DIRECTION('',(0.,0.,-1.));
#4468=DIRECTION('center_axis',(0.,0.,1.));
#4469=DIRECTION('ref_axis',(1.,0.,0.));
#5317=CARTESIAN_POINT('',(0.,0.,0.));
#5318=CARTESIAN_POINT('Origin',(6.5,-5.73205080756888,7.22132034));
#5319=CARTESIAN_POINT('',(6.89841665441537,-5.69649564641799,8.48132034));
#5320=CARTESIAN_POINT('',(6.89841665441537,-5.69649564641799,7.28132034));
#5321=CARTESIAN_POINT('',(6.89841665441537,-5.69649564641799,7.22132034));
#5322=CARTESIAN_POINT('',(6.33158334558463,-5.36923428297892,8.48132034));
#5323=CARTESIAN_POINT('Origin',(6.5,-5.73205080756888,8.48132034));
#5324=CARTESIAN_POINT('',(6.33158334558463,-5.36923428297892,7.28132034));
#5325=CARTESIAN_POINT('',(6.33158334558463,-5.36923428297892,7.22132034));
#5326=CARTESIAN_POINT('Origin',(6.5,-5.73205080756888,7.28132034));
#5327=CARTESIAN_POINT('Origin',(9.5,-4.,7.22132034));
#5328=CARTESIAN_POINT('',(9.27,-4.32726136343907,7.28132034));
#5329=CARTESIAN_POINT('',(9.27,-4.32726136343907,8.48132034));
#5330=CARTESIAN_POINT('',(9.27,-4.32726136343907,7.22132034));
#5331=CARTESIAN_POINT('',(9.27,-3.67273863656093,7.28132034));
#5332=CARTESIAN_POINT('Origin',(9.5,-4.,7.28132034));
#5333=CARTESIAN_POINT('',(9.27,-3.67273863656093,8.48132034));
#5334=CARTESIAN_POINT('',(9.27,-3.67273863656093,7.22132034));
#5335=CARTESIAN_POINT('Origin',(9.5,-4.,8.48132034));
#5336=CARTESIAN_POINT('Origin',(8.5,-2.26794919243112,7.22132034));
#5337=CARTESIAN_POINT('',(8.10158334558463,-2.30350435358201,8.48132034));
#5338=CARTESIAN_POINT('',(8.10158334558463,-2.30350435358201,7.28132034));
#5339=CARTESIAN_POINT('',(8.10158334558463,-2.30350435358201,7.22132034));
#5340=CARTESIAN_POINT('',(8.66841665441537,-2.63076571702108,8.48132034));
#5341=CARTESIAN_POINT('Origin',(8.5,-2.26794919243112,8.48132034));
#5342=CARTESIAN_POINT('',(8.66841665441537,-2.63076571702108,7.28132034));
#5343=CARTESIAN_POINT('',(8.66841665441537,-2.63076571702108,7.22132034));
#5344=CARTESIAN_POINT('Origin',(8.5,-2.26794919243112,7.28132034));
#5345=CARTESIAN_POINT('Origin',(6.5,-2.26794919243112,7.22132034));
#5346=CARTESIAN_POINT('',(6.33158334558463,-2.63076571702108,8.48132034));
#5347=CARTESIAN_POINT('',(6.33158334558463,-2.63076571702108,7.28132034));
#5348=CARTESIAN_POINT('',(6.33158334558463,-2.63076571702108,7.22132034));
#5349=CARTESIAN_POINT('',(6.89841665441537,-2.30350435358201,8.48132034));
#5350=CARTESIAN_POINT('Origin',(6.5,-2.26794919243112,8.48132034));
#5351=CARTESIAN_POINT('',(6.89841665441537,-2.30350435358201,7.28132034));
#5352=CARTESIAN_POINT('',(6.89841665441537,-2.30350435358201,7.22132034));
#5353=CARTESIAN_POINT('Origin',(6.5,-2.26794919243112,7.28132034));
#5354=CARTESIAN_POINT('Origin',(5.5,-4.,7.22132034));
#5355=CARTESIAN_POINT('',(5.73,-4.32726136343907,8.48132034));
#5356=CARTESIAN_POINT('',(5.73,-4.32726136343907,7.28132034));
#5357=CARTESIAN_POINT('',(5.73,-4.32726136343907,7.22132034));
#5358=CARTESIAN_POINT('',(5.73,-3.67273863656093,8.48132034));
#5359=CARTESIAN_POINT('Origin',(5.5,-4.,8.48132034));
#5360=CARTESIAN_POINT('',(5.73,-3.67273863656093,7.28132034));
#5361=CARTESIAN_POINT('',(5.73,-3.67273863656093,7.22132034));
#5362=CARTESIAN_POINT('Origin',(5.5,-4.,7.28132034));
#5363=CARTESIAN_POINT('Origin',(8.5,-5.73205080756888,7.22132034));
#5364=CARTESIAN_POINT('',(8.66841665441537,-5.36923428297892,8.48132034));
#5365=CARTESIAN_POINT('',(8.66841665441537,-5.36923428297892,7.28132034));
#5366=CARTESIAN_POINT('',(8.66841665441537,-5.36923428297892,7.22132034));
#5367=CARTESIAN_POINT('',(8.10158334558463,-5.69649564641799,8.48132034));
#5368=CARTESIAN_POINT('Origin',(8.5,-5.73205080756888,8.48132034));
#5369=CARTESIAN_POINT('',(8.10158334558463,-5.69649564641799,7.28132034));
#5370=CARTESIAN_POINT('',(8.10158334558463,-5.69649564641799,7.22132034));
#5371=CARTESIAN_POINT('Origin',(8.5,-5.73205080756888,7.28132034));
#5372=CARTESIAN_POINT('Origin',(7.5,-4.,8.48132034));
#5373=CARTESIAN_POINT('Origin',(7.5,-4.,8.48132034));
#5374=CARTESIAN_POINT('Origin',(7.5,-4.,8.48132034));
#5375=CARTESIAN_POINT('Origin',(7.5,-4.,8.48132034));
#5376=CARTESIAN_POINT('Origin',(7.5,-4.,8.48132034));
#5377=CARTESIAN_POINT('Origin',(7.5,-4.,8.48132034));
#5378=CARTESIAN_POINT('Origin',(7.5,-4.,8.48132034));
#5379=CARTESIAN_POINT('',(7.075,-4.,8.48132034));
#5380=CARTESIAN_POINT('Origin',(7.5,-4.,8.48132034));
#5381=CARTESIAN_POINT('Origin',(7.5,-4.,7.28132034));
#5382=CARTESIAN_POINT('Origin',(7.5,-4.,7.28132034));
#5383=CARTESIAN_POINT('Origin',(7.5,-4.,7.28132034));
#5384=CARTESIAN_POINT('Origin',(7.5,-4.,7.28132034));
#5385=CARTESIAN_POINT('Origin',(7.5,-4.,7.28132034));
#5386=CARTESIAN_POINT('Origin',(7.5,-4.,7.28132034));
#5387=CARTESIAN_POINT('Origin',(7.5,-4.,7.28132034));
#5388=CARTESIAN_POINT('Origin',(7.5,-4.,7.28132034));
#5389=CARTESIAN_POINT('Origin',(7.5,-4.,7.28132034));
#5390=CARTESIAN_POINT('Origin',(7.5,-4.,7.28132034));
#5391=CARTESIAN_POINT('Origin',(7.5,-4.,7.28132034));
#5392=CARTESIAN_POINT('Origin',(7.5,-4.,7.28132034));
#5393=CARTESIAN_POINT('Origin',(7.87527767497326,-3.35,7.27132034));
#5394=CARTESIAN_POINT('',(7.87527767497326,-3.35,7.28132034));
#5395=CARTESIAN_POINT('',(7.12472232502674,-3.35,7.28132034));
#5396=CARTESIAN_POINT('',(7.68763883748663,-3.35,7.28132034));
#5397=CARTESIAN_POINT('',(7.87527767497326,-3.35,7.97132034));
#5398=CARTESIAN_POINT('',(7.87527767497326,-3.35,7.27132034));
#5399=CARTESIAN_POINT('',(7.12472232502674,-3.35,7.97132034));
#5400=CARTESIAN_POINT('',(7.87527767497326,-3.35,7.97132034));
#5401=CARTESIAN_POINT('',(7.12472232502674,-3.35,7.27132034));
#5402=CARTESIAN_POINT('Origin',(7.12472232502674,-3.35,7.27132034));
#5403=CARTESIAN_POINT('',(6.74944465005349,-4.,7.28132034));
#5404=CARTESIAN_POINT('',(7.03090290628343,-3.5125,7.28132034));
#5405=CARTESIAN_POINT('',(6.74944465005349,-4.,7.97132034));
#5406=CARTESIAN_POINT('',(7.12472232502674,-3.35,7.97132034));
#5407=CARTESIAN_POINT('',(6.74944465005349,-4.,7.27132034));
#5408=CARTESIAN_POINT('Origin',(6.74944465005349,-4.,7.27132034));
#5409=CARTESIAN_POINT('',(7.12472232502674,-4.65,7.28132034));
#5410=CARTESIAN_POINT('',(6.8432640687968,-4.1625,7.28132034));
#5411=CARTESIAN_POINT('',(7.12472232502674,-4.65,7.97132034));
#5412=CARTESIAN_POINT('',(6.74944465005349,-4.,7.97132034));
#5413=CARTESIAN_POINT('',(7.12472232502674,-4.65,7.27132034));
#5414=CARTESIAN_POINT('Origin',(7.12472232502674,-4.65,7.27132034));
#5415=CARTESIAN_POINT('',(7.87527767497326,-4.65,7.28132034));
#5416=CARTESIAN_POINT('',(7.31236116251337,-4.65,7.28132034));
#5417=CARTESIAN_POINT('',(7.87527767497326,-4.65,7.97132034));
#5418=CARTESIAN_POINT('',(7.12472232502674,-4.65,7.97132034));
#5419=CARTESIAN_POINT('',(7.87527767497326,-4.65,7.27132034));
#5420=CARTESIAN_POINT('Origin',(8.25055534994651,-4.,7.27132034));
#5421=CARTESIAN_POINT('',(8.25055534994651,-4.,7.28132034));
#5422=CARTESIAN_POINT('',(8.1567359312032,-3.8375,7.28132034));
#5423=CARTESIAN_POINT('',(8.25055534994651,-4.,7.97132034));
#5424=CARTESIAN_POINT('',(8.25055534994651,-4.,7.27132034));
#5425=CARTESIAN_POINT('',(8.25055534994651,-4.,7.97132034));
#5426=CARTESIAN_POINT('Origin',(7.87527767497326,-4.65,7.27132034));
#5427=CARTESIAN_POINT('',(7.96909709371657,-4.4875,7.28132034));
#5428=CARTESIAN_POINT('',(7.87527767497326,-4.65,7.97132034));
#5429=CARTESIAN_POINT('Origin',(7.5,-4.,7.97132034));
#5430=CARTESIAN_POINT('',(7.075,-4.,7.97132034));
#5431=CARTESIAN_POINT('Origin',(7.5,-4.,7.97132034));
#5432=CARTESIAN_POINT('Origin',(7.5,-4.,7.28132034));
#5433=CARTESIAN_POINT('',(7.075,-4.,7.28132034));
#5434=CARTESIAN_POINT('Origin',(7.5,-4.,7.28132034));
#5474=UNCERTAINTY_MEASURE_WITH_UNIT(LENGTH_MEASURE(0.001),#5493,
'DISTANCE_ACCURACY_VALUE',
'Maximum model space distance between geometric entities at asserted c
onnectivities');
#5475=UNCERTAINTY_MEASURE_WITH_UNIT(LENGTH_MEASURE(0.001),#5493,
'DISTANCE_ACCURACY_VALUE',
'Maximum model space distance between geometric entities at asserted c
onnectivities');
#5491=(
GEOMETRIC_REPRESENTATION_CONTEXT(3)
GLOBAL_UNCERTAINTY_ASSIGNED_CONTEXT((#5474))
GLOBAL_UNIT_ASSIGNED_CONTEXT((#5493,#5495,#5496))
REPRESENTATION_CONTEXT('','3D')
);
#5492=(
GEOMETRIC_REPRESENTATION_CONTEXT(3)
GLOBAL_UNCERTAINTY_ASSIGNED_CONTEXT((#5475))
GLOBAL_UNIT_ASSIGNED_CONTEXT((#5493,#5495,#5496))
REPRESENTATION_CONTEXT('','3D')
);
#5493=(
LENGTH_UNIT()
NAMED_UNIT(*)
SI_UNIT(.CENTI.,.METRE.)
);
#5495=(
NAMED_UNIT(*)
PLANE_ANGLE_UNIT()
SI_UNIT($,.RADIAN.)
);
#5496=(
NAMED_UNIT(*)
SI_UNIT($,.STERADIAN.)
SOLID_ANGLE_UNIT()
);
#5512=SHAPE_DEFINITION_REPRESENTATION(#5537,#5577);
#5537=PRODUCT_DEFINITION_SHAPE('',$,#5594);
#5577=SHAPE_REPRESENTATION('',(#3532),#5491);
#5578=PRODUCT_DEFINITION_CONTEXT('part definition',#5628,'design');
#5594=PRODUCT_DEFINITION('Captive-nut hand knob',
'Captive-nut hand knob',#5610,#5578);
#5610=PRODUCT_DEFINITION_FORMATION('',$,#5645);
#5628=APPLICATION_CONTEXT(
'Core Data for Automotive Mechanical Design Process');
#5629=PRODUCT_CONTEXT('part definition',#5628,'mechanical');
#5645=PRODUCT('Captive-nut hand knob','Captive-nut hand knob',
'Captive-nut hand knob',(#5629));
#5702=COLOUR_RGB('Black',0.12,0.14,0.17);
#5703=FILL_AREA_STYLE_COLOUR('',#5702);
#5704=FILL_AREA_STYLE('',(#5703));
#5705=SURFACE_STYLE_FILL_AREA(#5704);
#5706=SURFACE_SIDE_STYLE('',(#5705));
#5707=SURFACE_STYLE_USAGE(.BOTH.,#5706);
#5708=PRESENTATION_STYLE_ASSIGNMENT((#5707));
ENDSEC;
END-ISO-10303-21;
